ISO-10303-21;
HEADER;
/* Generated by software containing ST-Developer
 * from STEP Tools, Inc. (www.steptools.com) 
 */

FILE_DESCRIPTION(
/* description */ (''),
/* implementation_level */ '2;1');

FILE_NAME(
/* name */ 'BOLT.step',
/* time_stamp */ '2026-10-04T02:10:06-07:00',
/* author */ (''),
/* organization */ (''),
/* preprocessor_version */ 'ST-DEVELOPER v20.2',
/* originating_system */ 'Autodesk Translation Framework v15.15.0.0',
/* authorisation */ '');

FILE_SCHEMA (('AUTOMOTIVE_DESIGN { 1 0 10303 214 3 1 1 }'));
ENDSEC;

DATA;
#10=MECHANICAL_DESIGN_GEOMETRIC_PRESENTATION_REPRESENTATION('',(#151),#9668);
#107=(
BOUNDED_CURVE()
B_SPLINE_CURVE(2,(#9539,#9540,#9541),.UNSPECIFIED.,.F.,.F.)
B_SPLINE_CURVE_WITH_KNOTS((3,3),(1.0700801839918,2.01951998481884),
 .UNSPECIFIED.)
CURVE()
GEOMETRIC_REPRESENTATION_ITEM()
RATIONAL_B_SPLINE_CURVE((1.37478521766072,1.48112522432469,1.48112522432469))
REPRESENTATION_ITEM('')
);
#108=(
BOUNDED_CURVE()
B_SPLINE_CURVE(2,(#9548,#9549,#9550),.UNSPECIFIED.,.F.,.F.)
B_SPLINE_CURVE_WITH_KNOTS((3,3),(2.01951998481884,2.96895978564587),
 .UNSPECIFIED.)
CURVE()
GEOMETRIC_REPRESENTATION_ITEM()
RATIONAL_B_SPLINE_CURVE((1.48112522432469,1.48112522432469,1.37478521766072))
REPRESENTATION_ITEM('')
);
#109=(
BOUNDED_CURVE()
B_SPLINE_CURVE(2,(#9553,#9554,#9555),.UNSPECIFIED.,.F.,.F.)
B_SPLINE_CURVE_WITH_KNOTS((3,3),(1.0700801839918,2.01951998481884),
 .UNSPECIFIED.)
CURVE()
GEOMETRIC_REPRESENTATION_ITEM()
RATIONAL_B_SPLINE_CURVE((1.37478521766072,1.48112522432469,1.48112522432469))
REPRESENTATION_ITEM('')
);
#110=(
BOUNDED_CURVE()
B_SPLINE_CURVE(2,(#9560,#9561,#9562),.UNSPECIFIED.,.F.,.F.)
B_SPLINE_CURVE_WITH_KNOTS((3,3),(2.01951998481884,2.96895978564588),
 .UNSPECIFIED.)
CURVE()
GEOMETRIC_REPRESENTATION_ITEM()
RATIONAL_B_SPLINE_CURVE((1.48112522432469,1.48112522432469,1.37478521766072))
REPRESENTATION_ITEM('')
);
#111=(
BOUNDED_CURVE()
B_SPLINE_CURVE(2,(#9565,#9566,#9567),.UNSPECIFIED.,.F.,.F.)
B_SPLINE_CURVE_WITH_KNOTS((3,3),(1.0700801839918,2.01951998481883),
 .UNSPECIFIED.)
CURVE()
GEOMETRIC_REPRESENTATION_ITEM()
RATIONAL_B_SPLINE_CURVE((1.37478521766072,1.48112522432469,1.48112522432469))
REPRESENTATION_ITEM('')
);
#112=(
BOUNDED_CURVE()
B_SPLINE_CURVE(2,(#9572,#9573,#9574),.UNSPECIFIED.,.F.,.F.)
B_SPLINE_CURVE_WITH_KNOTS((3,3),(2.01951998481883,2.96895978564588),
 .UNSPECIFIED.)
CURVE()
GEOMETRIC_REPRESENTATION_ITEM()
RATIONAL_B_SPLINE_CURVE((1.48112522432469,1.48112522432469,1.37478521766072))
REPRESENTATION_ITEM('')
);
#113=(
BOUNDED_CURVE()
B_SPLINE_CURVE(2,(#9577,#9578,#9579),.UNSPECIFIED.,.F.,.F.)
B_SPLINE_CURVE_WITH_KNOTS((3,3),(1.0700801839918,2.01951998481884),
 .UNSPECIFIED.)
CURVE()
GEOMETRIC_REPRESENTATION_ITEM()
RATIONAL_B_SPLINE_CURVE((1.37478521766072,1.48112522432469,1.48112522432469))
REPRESENTATION_ITEM('')
);
#114=(
BOUNDED_CURVE()
B_SPLINE_CURVE(2,(#9584,#9585,#9586),.UNSPECIFIED.,.F.,.F.)
B_SPLINE_CURVE_WITH_KNOTS((3,3),(2.01951998481884,2.96895978564587),
 .UNSPECIFIED.)
CURVE()
GEOMETRIC_REPRESENTATION_ITEM()
RATIONAL_B_SPLINE_CURVE((1.48112522432469,1.48112522432469,1.37478521766072))
REPRESENTATION_ITEM('')
);
#115=(
BOUNDED_CURVE()
B_SPLINE_CURVE(2,(#9589,#9590,#9591),.UNSPECIFIED.,.F.,.F.)
B_SPLINE_CURVE_WITH_KNOTS((3,3),(1.0700801839918,2.01951998481884),
 .UNSPECIFIED.)
CURVE()
GEOMETRIC_REPRESENTATION_ITEM()
RATIONAL_B_SPLINE_CURVE((1.37478521766072,1.48112522432469,1.48112522432469))
REPRESENTATION_ITEM('')
);
#116=(
BOUNDED_CURVE()
B_SPLINE_CURVE(2,(#9596,#9597,#9598),.UNSPECIFIED.,.F.,.F.)
B_SPLINE_CURVE_WITH_KNOTS((3,3),(2.01951998481884,2.96895978564587),
 .UNSPECIFIED.)
CURVE()
GEOMETRIC_REPRESENTATION_ITEM()
RATIONAL_B_SPLINE_CURVE((1.48112522432469,1.48112522432469,1.37478521766072))
REPRESENTATION_ITEM('')
);
#117=(
BOUNDED_CURVE()
B_SPLINE_CURVE(2,(#9601,#9602,#9603),.UNSPECIFIED.,.F.,.F.)
B_SPLINE_CURVE_WITH_KNOTS((3,3),(1.0700801839918,2.01951998481884),
 .UNSPECIFIED.)
CURVE()
GEOMETRIC_REPRESENTATION_ITEM()
RATIONAL_B_SPLINE_CURVE((1.37478521766072,1.48112522432469,1.48112522432469))
REPRESENTATION_ITEM('')
);
#118=(
BOUNDED_CURVE()
B_SPLINE_CURVE(2,(#9605,#9606,#9607),.UNSPECIFIED.,.F.,.F.)
B_SPLINE_CURVE_WITH_KNOTS((3,3),(2.01951998481884,2.96895978564587),
 .UNSPECIFIED.)
CURVE()
GEOMETRIC_REPRESENTATION_ITEM()
RATIONAL_B_SPLINE_CURVE((1.48112522432469,1.48112522432469,1.37478521766072))
REPRESENTATION_ITEM('')
);
#129=SHAPE_REPRESENTATION_RELATIONSHIP('SRR','None',#9722,#140);
#140=ADVANCED_BREP_SHAPE_REPRESENTATION('',(#162),#9667);
#151=STYLED_ITEM('',(#9775),#162);
#162=MANIFOLD_SOLID_BREP('Body1',#3891);
#189=CONICAL_SURFACE('',#4442,10.3923048454133,0.78539816339745);
#190=CONICAL_SURFACE('',#4444,10.3923048454133,0.78539816339745);
#191=CONICAL_SURFACE('',#4446,10.3923048454133,0.78539816339745);
#192=CONICAL_SURFACE('',#4448,10.3923048454133,0.78539816339745);
#193=CONICAL_SURFACE('',#4450,10.3923048454133,0.78539816339745);
#194=CONICAL_SURFACE('',#4452,10.3923048454133,0.78539816339745);
#267=FACE_BOUND('',#1321,.T.);
#362=PLANE('',#4431);
#363=PLANE('',#4432);
#364=PLANE('',#4433);
#365=PLANE('',#4434);
#366=PLANE('',#4435);
#367=PLANE('',#4436);
#368=PLANE('',#4440);
#369=PLANE('',#4441);
#370=PLANE('',#4454);
#549=LINE('',#9543,#740);
#550=LINE('',#9545,#741);
#551=LINE('',#9547,#742);
#552=LINE('',#9557,#743);
#553=LINE('',#9559,#744);
#554=LINE('',#9569,#745);
#555=LINE('',#9571,#746);
#556=LINE('',#9581,#747);
#557=LINE('',#9583,#748);
#558=LINE('',#9593,#749);
#559=LINE('',#9595,#750);
#560=LINE('',#9604,#751);
#561=LINE('',#9612,#752);
#740=VECTOR('',#5483,7.39230484541327);
#741=VECTOR('',#5484,12.);
#742=VECTOR('',#5485,7.39230484541327);
#743=VECTOR('',#5488,12.);
#744=VECTOR('',#5489,7.39230484541327);
#745=VECTOR('',#5492,12.);
#746=VECTOR('',#5493,7.39230484541327);
#747=VECTOR('',#5496,12.);
#748=VECTOR('',#5497,7.39230484541327);
#749=VECTOR('',#5500,12.);
#750=VECTOR('',#5501,7.39230484541327);
#751=VECTOR('',#5504,12.);
#752=VECTOR('',#5509,6.);
#809=CYLINDRICAL_SURFACE('',#4437,6.);
#1017=FACE_OUTER_BOUND('',#1312,.T.);
#1018=FACE_OUTER_BOUND('',#1313,.T.);
#1019=FACE_OUTER_BOUND('',#1314,.T.);
#1020=FACE_OUTER_BOUND('',#1315,.T.);
#1021=FACE_OUTER_BOUND('',#1316,.T.);
#1022=FACE_OUTER_BOUND('',#1317,.T.);
#1023=FACE_OUTER_BOUND('',#1318,.T.);
#1024=FACE_OUTER_BOUND('',#1319,.T.);
#1025=FACE_OUTER_BOUND('',#1320,.T.);
#1026=FACE_OUTER_BOUND('',#1322,.T.);
#1027=FACE_OUTER_BOUND('',#1323,.T.);
#1028=FACE_OUTER_BOUND('',#1324,.T.);
#1029=FACE_OUTER_BOUND('',#1325,.T.);
#1030=FACE_OUTER_BOUND('',#1326,.T.);
#1031=FACE_OUTER_BOUND('',#1327,.T.);
#1032=FACE_OUTER_BOUND('',#1328,.T.);
#1312=EDGE_LOOP('',(#3569,#3570,#3571,#3572,#3573));
#1313=EDGE_LOOP('',(#3574,#3575,#3576,#3577,#3578));
#1314=EDGE_LOOP('',(#3579,#3580,#3581,#3582,#3583));
#1315=EDGE_LOOP('',(#3584,#3585,#3586,#3587,#3588));
#1316=EDGE_LOOP('',(#3589,#3590,#3591,#3592,#3593));
#1317=EDGE_LOOP('',(#3594,#3595,#3596,#3597,#3598));
#1318=EDGE_LOOP('',(#3599,#3600,#3601,#3602));
#1319=EDGE_LOOP('',(#3603));
#1320=EDGE_LOOP('',(#3604,#3605,#3606,#3607,#3608,#3609));
#1321=EDGE_LOOP('',(#3610));
#1322=EDGE_LOOP('',(#3611,#3612,#3613));
#1323=EDGE_LOOP('',(#3614,#3615,#3616));
#1324=EDGE_LOOP('',(#3617,#3618,#3619));
#1325=EDGE_LOOP('',(#3620,#3621,#3622));
#1326=EDGE_LOOP('',(#3623,#3624,#3625));
#1327=EDGE_LOOP('',(#3626,#3627,#3628));
#1328=EDGE_LOOP('',(#3629,#3630,#3631,#3632,#3633,#3634));
#1633=CIRCLE('',#4438,6.);
#1634=CIRCLE('',#4439,6.);
#1635=CIRCLE('',#4443,10.3923048454133);
#1636=CIRCLE('',#4445,10.3923048454133);
#1637=CIRCLE('',#4447,10.3923048454133);
#1638=CIRCLE('',#4449,10.3923048454133);
#1639=CIRCLE('',#4451,10.3923048454133);
#1640=CIRCLE('',#4453,10.3923048454133);
#1974=VERTEX_POINT('',#9537);
#1975=VERTEX_POINT('',#9538);
#1976=VERTEX_POINT('',#9542);
#1977=VERTEX_POINT('',#9544);
#1978=VERTEX_POINT('',#9546);
#1979=VERTEX_POINT('',#9552);
#1980=VERTEX_POINT('',#9556);
#1981=VERTEX_POINT('',#9558);
#1982=VERTEX_POINT('',#9564);
#1983=VERTEX_POINT('',#9568);
#1984=VERTEX_POINT('',#9570);
#1985=VERTEX_POINT('',#9576);
#1986=VERTEX_POINT('',#9580);
#1987=VERTEX_POINT('',#9582);
#1988=VERTEX_POINT('',#9588);
#1989=VERTEX_POINT('',#9592);
#1990=VERTEX_POINT('',#9594);
#1991=VERTEX_POINT('',#9600);
#1992=VERTEX_POINT('',#9609);
#1993=VERTEX_POINT('',#9611);
#2508=EDGE_CURVE('',#1974,#1975,#107,.T.);
#2509=EDGE_CURVE('',#1974,#1976,#549,.T.);
#2510=EDGE_CURVE('',#1976,#1977,#550,.T.);
#2511=EDGE_CURVE('',#1978,#1977,#551,.T.);
#2512=EDGE_CURVE('',#1975,#1978,#108,.T.);
#2513=EDGE_CURVE('',#1978,#1979,#109,.T.);
#2514=EDGE_CURVE('',#1977,#1980,#552,.T.);
#2515=EDGE_CURVE('',#1981,#1980,#553,.T.);
#2516=EDGE_CURVE('',#1979,#1981,#110,.T.);
#2517=EDGE_CURVE('',#1981,#1982,#111,.T.);
#2518=EDGE_CURVE('',#1980,#1983,#554,.T.);
#2519=EDGE_CURVE('',#1984,#1983,#555,.T.);
#2520=EDGE_CURVE('',#1982,#1984,#112,.T.);
#2521=EDGE_CURVE('',#1984,#1985,#113,.T.);
#2522=EDGE_CURVE('',#1983,#1986,#556,.T.);
#2523=EDGE_CURVE('',#1987,#1986,#557,.T.);
#2524=EDGE_CURVE('',#1985,#1987,#114,.T.);
#2525=EDGE_CURVE('',#1987,#1988,#115,.T.);
#2526=EDGE_CURVE('',#1986,#1989,#558,.T.);
#2527=EDGE_CURVE('',#1990,#1989,#559,.T.);
#2528=EDGE_CURVE('',#1988,#1990,#116,.T.);
#2529=EDGE_CURVE('',#1990,#1991,#117,.T.);
#2530=EDGE_CURVE('',#1989,#1976,#560,.T.);
#2531=EDGE_CURVE('',#1991,#1974,#118,.T.);
#2532=EDGE_CURVE('',#1992,#1992,#1633,.T.);
#2533=EDGE_CURVE('',#1992,#1993,#561,.T.);
#2534=EDGE_CURVE('',#1993,#1993,#1634,.T.);
#2535=EDGE_CURVE('',#1988,#1991,#1635,.T.);
#2536=EDGE_CURVE('',#1985,#1988,#1636,.T.);
#2537=EDGE_CURVE('',#1982,#1985,#1637,.T.);
#2538=EDGE_CURVE('',#1979,#1982,#1638,.T.);
#2539=EDGE_CURVE('',#1975,#1979,#1639,.T.);
#2540=EDGE_CURVE('',#1991,#1975,#1640,.T.);
#3569=ORIENTED_EDGE('',*,*,#2508,.F.);
#3570=ORIENTED_EDGE('',*,*,#2509,.T.);
#3571=ORIENTED_EDGE('',*,*,#2510,.T.);
#3572=ORIENTED_EDGE('',*,*,#2511,.F.);
#3573=ORIENTED_EDGE('',*,*,#2512,.F.);
#3574=ORIENTED_EDGE('',*,*,#2513,.F.);
#3575=ORIENTED_EDGE('',*,*,#2511,.T.);
#3576=ORIENTED_EDGE('',*,*,#2514,.T.);
#3577=ORIENTED_EDGE('',*,*,#2515,.F.);
#3578=ORIENTED_EDGE('',*,*,#2516,.F.);
#3579=ORIENTED_EDGE('',*,*,#2517,.F.);
#3580=ORIENTED_EDGE('',*,*,#2515,.T.);
#3581=ORIENTED_EDGE('',*,*,#2518,.T.);
#3582=ORIENTED_EDGE('',*,*,#2519,.F.);
#3583=ORIENTED_EDGE('',*,*,#2520,.F.);
#3584=ORIENTED_EDGE('',*,*,#2521,.F.);
#3585=ORIENTED_EDGE('',*,*,#2519,.T.);
#3586=ORIENTED_EDGE('',*,*,#2522,.T.);
#3587=ORIENTED_EDGE('',*,*,#2523,.F.);
#3588=ORIENTED_EDGE('',*,*,#2524,.F.);
#3589=ORIENTED_EDGE('',*,*,#2525,.F.);
#3590=ORIENTED_EDGE('',*,*,#2523,.T.);
#3591=ORIENTED_EDGE('',*,*,#2526,.T.);
#3592=ORIENTED_EDGE('',*,*,#2527,.F.);
#3593=ORIENTED_EDGE('',*,*,#2528,.F.);
#3594=ORIENTED_EDGE('',*,*,#2529,.F.);
#3595=ORIENTED_EDGE('',*,*,#2527,.T.);
#3596=ORIENTED_EDGE('',*,*,#2530,.T.);
#3597=ORIENTED_EDGE('',*,*,#2509,.F.);
#3598=ORIENTED_EDGE('',*,*,#2531,.F.);
#3599=ORIENTED_EDGE('',*,*,#2532,.T.);
#3600=ORIENTED_EDGE('',*,*,#2533,.T.);
#3601=ORIENTED_EDGE('',*,*,#2534,.F.);
#3602=ORIENTED_EDGE('',*,*,#2533,.F.);
#3603=ORIENTED_EDGE('',*,*,#2532,.F.);
#3604=ORIENTED_EDGE('',*,*,#2510,.F.);
#3605=ORIENTED_EDGE('',*,*,#2530,.F.);
#3606=ORIENTED_EDGE('',*,*,#2526,.F.);
#3607=ORIENTED_EDGE('',*,*,#2522,.F.);
#3608=ORIENTED_EDGE('',*,*,#2518,.F.);
#3609=ORIENTED_EDGE('',*,*,#2514,.F.);
#3610=ORIENTED_EDGE('',*,*,#2534,.T.);
#3611=ORIENTED_EDGE('',*,*,#2528,.T.);
#3612=ORIENTED_EDGE('',*,*,#2529,.T.);
#3613=ORIENTED_EDGE('',*,*,#2535,.F.);
#3614=ORIENTED_EDGE('',*,*,#2524,.T.);
#3615=ORIENTED_EDGE('',*,*,#2525,.T.);
#3616=ORIENTED_EDGE('',*,*,#2536,.F.);
#3617=ORIENTED_EDGE('',*,*,#2520,.T.);
#3618=ORIENTED_EDGE('',*,*,#2521,.T.);
#3619=ORIENTED_EDGE('',*,*,#2537,.F.);
#3620=ORIENTED_EDGE('',*,*,#2516,.T.);
#3621=ORIENTED_EDGE('',*,*,#2517,.T.);
#3622=ORIENTED_EDGE('',*,*,#2538,.F.);
#3623=ORIENTED_EDGE('',*,*,#2512,.T.);
#3624=ORIENTED_EDGE('',*,*,#2513,.T.);
#3625=ORIENTED_EDGE('',*,*,#2539,.F.);
#3626=ORIENTED_EDGE('',*,*,#2508,.T.);
#3627=ORIENTED_EDGE('',*,*,#2540,.F.);
#3628=ORIENTED_EDGE('',*,*,#2531,.T.);
#3629=ORIENTED_EDGE('',*,*,#2535,.T.);
#3630=ORIENTED_EDGE('',*,*,#2540,.T.);
#3631=ORIENTED_EDGE('',*,*,#2539,.T.);
#3632=ORIENTED_EDGE('',*,*,#2538,.T.);
#3633=ORIENTED_EDGE('',*,*,#2537,.T.);
#3634=ORIENTED_EDGE('',*,*,#2536,.T.);
#3865=ADVANCED_FACE('',(#1017),#362,.F.);
#3866=ADVANCED_FACE('',(#1018),#363,.F.);
#3867=ADVANCED_FACE('',(#1019),#364,.F.);
#3868=ADVANCED_FACE('',(#1020),#365,.F.);
#3869=ADVANCED_FACE('',(#1021),#366,.F.);
#3870=ADVANCED_FACE('',(#1022),#367,.F.);
#3871=ADVANCED_FACE('',(#1023),#809,.T.);
#3872=ADVANCED_FACE('',(#1024),#368,.F.);
#3873=ADVANCED_FACE('',(#1025,#267),#369,.F.);
#3874=ADVANCED_FACE('',(#1026),#189,.T.);
#3875=ADVANCED_FACE('',(#1027),#190,.T.);
#3876=ADVANCED_FACE('',(#1028),#191,.T.);
#3877=ADVANCED_FACE('',(#1029),#192,.T.);
#3878=ADVANCED_FACE('',(#1030),#193,.T.);
#3879=ADVANCED_FACE('',(#1031),#194,.T.);
#3880=ADVANCED_FACE('',(#1032),#370,.T.);
#3891=CLOSED_SHELL('',(#3865,#3866,#3867,#3868,#3869,#3870,#3871,#3872,
#3873,#3874,#3875,#3876,#3877,#3878,#3879,#3880));
#4430=AXIS2_PLACEMENT_3D('',#9535,#5479,#5480);
#4431=AXIS2_PLACEMENT_3D('',#9536,#5481,#5482);
#4432=AXIS2_PLACEMENT_3D('',#9551,#5486,#5487);
#4433=AXIS2_PLACEMENT_3D('',#9563,#5490,#5491);
#4434=AXIS2_PLACEMENT_3D('',#9575,#5494,#5495);
#4435=AXIS2_PLACEMENT_3D('',#9587,#5498,#5499);
#4436=AXIS2_PLACEMENT_3D('',#9599,#5502,#5503);
#4437=AXIS2_PLACEMENT_3D('',#9608,#5505,#5506);
#4438=AXIS2_PLACEMENT_3D('',#9610,#5507,#5508);
#4439=AXIS2_PLACEMENT_3D('',#9613,#5510,#5511);
#4440=AXIS2_PLACEMENT_3D('',#9614,#5512,#5513);
#4441=AXIS2_PLACEMENT_3D('',#9615,#5514,#5515);
#4442=AXIS2_PLACEMENT_3D('',#9616,#5516,#5517);
#4443=AXIS2_PLACEMENT_3D('',#9617,#5518,#5519);
#4444=AXIS2_PLACEMENT_3D('',#9618,#5520,#5521);
#4445=AXIS2_PLACEMENT_3D('',#9619,#5522,#5523);
#4446=AXIS2_PLACEMENT_3D('',#9620,#5524,#5525);
#4447=AXIS2_PLACEMENT_3D('',#9621,#5526,#5527);
#4448=AXIS2_PLACEMENT_3D('',#9622,#5528,#5529);
#4449=AXIS2_PLACEMENT_3D('',#9623,#5530,#5531);
#4450=AXIS2_PLACEMENT_3D('',#9624,#5532,#5533);
#4451=AXIS2_PLACEMENT_3D('',#9625,#5534,#5535);
#4452=AXIS2_PLACEMENT_3D('',#9626,#5536,#5537);
#4453=AXIS2_PLACEMENT_3D('',#9627,#5538,#5539);
#4454=AXIS2_PLACEMENT_3D('',#9628,#5540,#5541);
#5479=DIRECTION('axis',(0.,0.,1.));
#5480=DIRECTION('refdir',(1.,0.,0.));
#5481=DIRECTION('center_axis',(-0.866025403784439,0.,-0.5));
#5482=DIRECTION('ref_axis',(-0.5,0.,0.866025403784439));
#5483=DIRECTION('',(0.,-1.,0.));
#5484=DIRECTION('',(0.5,0.,-0.866025403784439));
#5485=DIRECTION('',(0.,-1.,0.));
#5486=DIRECTION('center_axis',(-0.866025403784439,0.,0.5));
#5487=DIRECTION('ref_axis',(0.5,0.,0.866025403784439));
#5488=DIRECTION('',(-0.5,0.,-0.866025403784439));
#5489=DIRECTION('',(0.,-1.,0.));
#5490=DIRECTION('center_axis',(-1.44560289664734E-16,0.,1.));
#5491=DIRECTION('ref_axis',(1.,0.,1.44560289664734E-16));
#5492=DIRECTION('',(-1.,0.,-1.85037170770859E-16));
#5493=DIRECTION('',(0.,-1.,0.));
#5494=DIRECTION('center_axis',(0.866025403784439,0.,0.5));
#5495=DIRECTION('ref_axis',(0.5,0.,-0.866025403784439));
#5496=DIRECTION('',(-0.5,0.,0.866025403784439));
#5497=DIRECTION('',(0.,-1.,0.));
#5498=DIRECTION('center_axis',(0.866025403784439,0.,-0.5));
#5499=DIRECTION('ref_axis',(-0.5,0.,-0.866025403784439));
#5500=DIRECTION('',(0.5,0.,0.866025403784439));
#5501=DIRECTION('',(0.,-1.,0.));
#5502=DIRECTION('center_axis',(0.,0.,-1.));
#5503=DIRECTION('ref_axis',(-1.,0.,0.));
#5504=DIRECTION('',(1.,0.,0.));
#5505=DIRECTION('center_axis',(0.,-1.,0.));
#5506=DIRECTION('ref_axis',(0.,0.,-1.));
#5507=DIRECTION('center_axis',(0.,1.,0.));
#5508=DIRECTION('ref_axis',(0.,0.,1.));
#5509=DIRECTION('',(0.,1.,0.));
#5510=DIRECTION('center_axis',(0.,1.,0.));
#5511=DIRECTION('ref_axis',(0.,0.,1.));
#5512=DIRECTION('center_axis',(0.,1.,0.));
#5513=DIRECTION('ref_axis',(0.,0.,1.));
#5514=DIRECTION('center_axis',(0.,1.,0.));
#5515=DIRECTION('ref_axis',(0.,0.,1.));
#5516=DIRECTION('center_axis',(0.,-1.,0.));
#5517=DIRECTION('ref_axis',(0.,0.,1.));
#5518=DIRECTION('center_axis',(0.,1.,0.));
#5519=DIRECTION('ref_axis',(0.,0.,1.));
#5520=DIRECTION('center_axis',(0.,-1.,0.));
#5521=DIRECTION('ref_axis',(0.,0.,1.));
#5522=DIRECTION('center_axis',(0.,1.,0.));
#5523=DIRECTION('ref_axis',(0.,0.,1.));
#5524=DIRECTION('center_axis',(0.,-1.,0.));
#5525=DIRECTION('ref_axis',(0.,0.,1.));
#5526=DIRECTION('center_axis',(0.,1.,0.));
#5527=DIRECTION('ref_axis',(0.,0.,1.));
#5528=DIRECTION('center_axis',(0.,-1.,0.));
#5529=DIRECTION('ref_axis',(0.,0.,1.));
#5530=DIRECTION('center_axis',(0.,1.,0.));
#5531=DIRECTION('ref_axis',(0.,0.,1.));
#5532=DIRECTION('center_axis',(0.,-1.,0.));
#5533=DIRECTION('ref_axis',(0.,0.,1.));
#5534=DIRECTION('center_axis',(0.,1.,0.));
#5535=DIRECTION('ref_axis',(0.,0.,1.));
#5536=DIRECTION('center_axis',(0.,-1.,0.));
#5537=DIRECTION('ref_axis',(0.,0.,1.));
#5538=DIRECTION('center_axis',(0.,1.,0.));
#5539=DIRECTION('ref_axis',(0.,0.,1.));
#5540=DIRECTION('center_axis',(0.,1.,0.));
#5541=DIRECTION('ref_axis',(0.,0.,1.));
#9535=CARTESIAN_POINT('',(0.,0.,0.));
#9536=CARTESIAN_POINT('Origin',(6.00000000000001,41.,10.3923048454133));
#9537=CARTESIAN_POINT('',(6.00000000000001,39.3923048454133,10.3923048454133));
#9538=CARTESIAN_POINT('',(9.00000000000001,41.,5.19615242270664));
#9539=CARTESIAN_POINT('Ctrl Pts',(6.00000000000003,39.3923048454133,10.3923048454132));
#9540=CARTESIAN_POINT('Ctrl Pts',(7.60769515458675,41.,7.60769515458673));
#9541=CARTESIAN_POINT('Ctrl Pts',(9.00000000000001,41.,5.19615242270663));
#9542=CARTESIAN_POINT('',(6.00000000000001,32.,10.3923048454133));
#9543=CARTESIAN_POINT('',(6.00000000000001,39.3923048454133,10.3923048454133));
#9544=CARTESIAN_POINT('',(12.,32.,1.67859117701527E-16));
#9545=CARTESIAN_POINT('',(6.00000000000001,32.,10.3923048454133));
#9546=CARTESIAN_POINT('',(12.,39.3923048454133,9.21294328526909E-16));
#9547=CARTESIAN_POINT('',(12.,39.3923048454133,1.67859117701527E-16));
#9548=CARTESIAN_POINT('Ctrl Pts',(9.00000000000001,41.,5.19615242270663));
#9549=CARTESIAN_POINT('Ctrl Pts',(10.3923048454133,41.,2.78460969082656));
#9550=CARTESIAN_POINT('Ctrl Pts',(12.,39.3923048454133,7.39725942272692E-14));
#9551=CARTESIAN_POINT('Origin',(12.,41.,1.67859117701527E-16));
#9552=CARTESIAN_POINT('',(9.00000000000001,41.,-5.19615242270664));
#9553=CARTESIAN_POINT('Ctrl Pts',(12.,39.3923048454133,-3.52096627544644E-14));
#9554=CARTESIAN_POINT('Ctrl Pts',(10.3923048454133,41.,-2.78460969082656));
#9555=CARTESIAN_POINT('Ctrl Pts',(8.99999999999999,41.,-5.19615242270666));
#9556=CARTESIAN_POINT('',(6.00000000000001,32.,-10.3923048454133));
#9557=CARTESIAN_POINT('',(12.,32.,1.67859117701527E-16));
#9558=CARTESIAN_POINT('',(6.00000000000001,39.3923048454133,-10.3923048454133));
#9559=CARTESIAN_POINT('',(6.00000000000001,39.3923048454133,-10.3923048454133));
#9560=CARTESIAN_POINT('Ctrl Pts',(8.99999999999999,41.,-5.19615242270666));
#9561=CARTESIAN_POINT('Ctrl Pts',(7.60769515458674,41.,-7.60769515458675));
#9562=CARTESIAN_POINT('Ctrl Pts',(6.00000000000002,39.3923048454133,-10.3923048454133));
#9563=CARTESIAN_POINT('Origin',(6.00000000000001,41.,-10.3923048454133));
#9564=CARTESIAN_POINT('',(1.50231459873716E-15,41.,-10.3923048454133));
#9565=CARTESIAN_POINT('Ctrl Pts',(5.99999999999996,39.3923048454133,-10.3923048454133));
#9566=CARTESIAN_POINT('Ctrl Pts',(2.78460969082653,41.,-10.3923048454133));
#9567=CARTESIAN_POINT('Ctrl Pts',(3.47805489344055E-14,41.,-10.3923048454133));
#9568=CARTESIAN_POINT('',(-6.,32.,-10.3923048454133));
#9569=CARTESIAN_POINT('',(6.00000000000001,32.,-10.3923048454133));
#9570=CARTESIAN_POINT('',(-6.,39.3923048454133,-10.3923048454133));
#9571=CARTESIAN_POINT('',(-6.,39.3923048454133,-10.3923048454133));
#9572=CARTESIAN_POINT('Ctrl Pts',(3.47805489344055E-14,41.,-10.3923048454133));
#9573=CARTESIAN_POINT('Ctrl Pts',(-2.78460969082651,41.,-10.3923048454133));
#9574=CARTESIAN_POINT('Ctrl Pts',(-6.00000000000001,39.3923048454133,-10.3923048454133));
#9575=CARTESIAN_POINT('Origin',(-6.,41.,-10.3923048454133));
#9576=CARTESIAN_POINT('',(-9.00000000000001,41.,-5.19615242270664));
#9577=CARTESIAN_POINT('Ctrl Pts',(-6.00000000000002,39.3923048454133,-10.3923048454132));
#9578=CARTESIAN_POINT('Ctrl Pts',(-7.60769515458675,41.,-7.60769515458673));
#9579=CARTESIAN_POINT('Ctrl Pts',(-9.00000000000001,41.,-5.19615242270663));
#9580=CARTESIAN_POINT('',(-12.,32.,2.18193936935029E-15));
#9581=CARTESIAN_POINT('',(-6.,32.,-10.3923048454133));
#9582=CARTESIAN_POINT('',(-12.,39.3923048454133,7.91126054510164E-16));
#9583=CARTESIAN_POINT('',(-12.,39.3923048454133,2.18193936935029E-15));
#9584=CARTESIAN_POINT('Ctrl Pts',(-9.00000000000001,41.,-5.19615242270663));
#9585=CARTESIAN_POINT('Ctrl Pts',(-10.3923048454133,41.,-2.78460969082655));
#9586=CARTESIAN_POINT('Ctrl Pts',(-12.,39.3923048454133,-5.42681040619267E-14));
#9587=CARTESIAN_POINT('Origin',(-12.,41.,2.18193936935029E-15));
#9588=CARTESIAN_POINT('',(-9.00000000000001,41.,5.19615242270664));
#9589=CARTESIAN_POINT('Ctrl Pts',(-12.,39.3923048454133,3.45636138965843E-14));
#9590=CARTESIAN_POINT('Ctrl Pts',(-10.3923048454133,41.,2.78460969082656));
#9591=CARTESIAN_POINT('Ctrl Pts',(-8.99999999999999,41.,5.19615242270666));
#9592=CARTESIAN_POINT('',(-6.,32.,10.3923048454133));
#9593=CARTESIAN_POINT('',(-12.,32.,2.18193936935029E-15));
#9594=CARTESIAN_POINT('',(-6.,39.3923048454133,10.3923048454133));
#9595=CARTESIAN_POINT('',(-6.,39.3923048454133,10.3923048454133));
#9596=CARTESIAN_POINT('Ctrl Pts',(-8.99999999999999,41.,5.19615242270666));
#9597=CARTESIAN_POINT('Ctrl Pts',(-7.60769515458674,41.,7.60769515458673));
#9598=CARTESIAN_POINT('Ctrl Pts',(-6.00000000000003,39.3923048454133,10.3923048454132));
#9599=CARTESIAN_POINT('Origin',(-6.,41.,10.3923048454133));
#9600=CARTESIAN_POINT('',(0.,41.,10.3923048454133));
#9601=CARTESIAN_POINT('Ctrl Pts',(-5.99999999999996,39.3923048454133,10.3923048454133));
#9602=CARTESIAN_POINT('Ctrl Pts',(-2.7846096908265,41.,10.3923048454133));
#9603=CARTESIAN_POINT('Ctrl Pts',(1.67906098304027E-14,41.,10.3923048454133));
#9604=CARTESIAN_POINT('',(-6.,32.,10.3923048454133));
#9605=CARTESIAN_POINT('Ctrl Pts',(1.67906098304027E-14,41.,10.3923048454133));
#9606=CARTESIAN_POINT('Ctrl Pts',(2.78460969082651,41.,10.3923048454133));
#9607=CARTESIAN_POINT('Ctrl Pts',(5.99999999999992,39.3923048454133,10.3923048454133));
#9608=CARTESIAN_POINT('Origin',(0.,32.,0.));
#9609=CARTESIAN_POINT('',(0.,0.,6.));
#9610=CARTESIAN_POINT('Origin',(0.,0.,0.));
#9611=CARTESIAN_POINT('',(0.,32.,6.));
#9612=CARTESIAN_POINT('',(-7.34788079488412E-16,32.,6.));
#9613=CARTESIAN_POINT('Origin',(0.,32.,0.));
#9614=CARTESIAN_POINT('Origin',(0.,0.,0.));
#9615=CARTESIAN_POINT('Origin',(0.,32.,0.));
#9616=CARTESIAN_POINT('Origin',(0.,41.,0.));
#9617=CARTESIAN_POINT('Origin',(0.,41.,0.));
#9618=CARTESIAN_POINT('Origin',(0.,41.,0.));
#9619=CARTESIAN_POINT('Origin',(0.,41.,0.));
#9620=CARTESIAN_POINT('Origin',(0.,41.,0.));
#9621=CARTESIAN_POINT('Origin',(0.,41.,0.));
#9622=CARTESIAN_POINT('Origin',(0.,41.,0.));
#9623=CARTESIAN_POINT('Origin',(0.,41.,0.));
#9624=CARTESIAN_POINT('Origin',(0.,41.,0.));
#9625=CARTESIAN_POINT('Origin',(0.,41.,0.));
#9626=CARTESIAN_POINT('Origin',(0.,41.,0.));
#9627=CARTESIAN_POINT('Origin',(0.,41.,0.));
#9628=CARTESIAN_POINT('Origin',(0.,41.,0.));
#9654=UNCERTAINTY_MEASURE_WITH_UNIT(LENGTH_MEASURE(0.01),#9669,
'DISTANCE_ACCURACY_VALUE',
'Maximum model space distance between geometric entities at asserted c
onnectivities');
#9655=UNCERTAINTY_MEASURE_WITH_UNIT(LENGTH_MEASURE(0.01),#9669,
'DISTANCE_ACCURACY_VALUE',
'Maximum model space distance between geometric entities at asserted c
onnectivities');
#9667=(
GEOMETRIC_REPRESENTATION_CONTEXT(3)
GLOBAL_UNCERTAINTY_ASSIGNED_CONTEXT((#9654))
GLOBAL_UNIT_ASSIGNED_CONTEXT((#9669,#9671,#9672))
REPRESENTATION_CONTEXT('','3D')
);
#9668=(
GEOMETRIC_REPRESENTATION_CONTEXT(3)
GLOBAL_UNCERTAINTY_ASSIGNED_CONTEXT((#9655))
GLOBAL_UNIT_ASSIGNED_CONTEXT((#9669,#9671,#9672))
REPRESENTATION_CONTEXT('','3D')
);
#9669=(
LENGTH_UNIT()
NAMED_UNIT(*)
SI_UNIT(.MILLI.,.METRE.)
);
#9671=(
NAMED_UNIT(*)
PLANE_ANGLE_UNIT()
SI_UNIT($,.RADIAN.)
);
#9672=(
NAMED_UNIT(*)
SI_UNIT($,.STERADIAN.)
SOLID_ANGLE_UNIT()
);
#9684=SHAPE_DEFINITION_REPRESENTATION(#9696,#9722);
#9696=PRODUCT_DEFINITION_SHAPE('',$,#9735);
#9722=SHAPE_REPRESENTATION('',(#4430),#9667);
#9723=PRODUCT_DEFINITION_CONTEXT('part definition',#9761,'design');
#9735=PRODUCT_DEFINITION('2026-10-04-08-13-48-890','BOLT',#9747,#9723);
#9747=PRODUCT_DEFINITION_FORMATION('',$,#9774);
#9761=APPLICATION_CONTEXT(
'Core Data for Automotive Mechanical Design Process');
#9762=PRODUCT_CONTEXT('part definition',#9761,'mechanical');
#9774=PRODUCT('2026-10-04-08-13-48-890','BOLT','PART',(#9762));
#9775=PRESENTATION_STYLE_ASSIGNMENT((#9776));
#9776=SURFACE_STYLE_USAGE(.BOTH.,#9777);
#9777=SURFACE_SIDE_STYLE('',(#9778));
#9778=SURFACE_STYLE_FILL_AREA(#9779);
#9779=FILL_AREA_STYLE('Steel - Satin',(#9780));
#9780=FILL_AREA_STYLE_COLOUR('Steel - Satin',#9781);
#9781=COLOUR_RGB('Steel - Satin', 0.09019608, 0.27058824, 0.51372549);
ENDSEC;
END-ISO-10303-21;
